ISO-10303-21;
HEADER;
/* Generated by software containing ST-Developer
 * from STEP Tools, Inc. (www.steptools.com) 
 */

FILE_DESCRIPTION(
/* description */ (''),
/* implementation_level */ '2;1');

FILE_NAME(
/* name */ 'Screw.step',
/* time_stamp */ '2026-10-22T16:03:28+06:00',
/* author */ (''),
/* organization */ (''),
/* preprocessor_version */ 'ST-DEVELOPER v20.2',
/* originating_system */ 'Autodesk Translation Framework v15.15.0.0',
/* authorisation */ '');

FILE_SCHEMA (('AUTOMOTIVE_DESIGN { 1 0 10303 214 3 1 1 }'));
ENDSEC;

DATA;
#10=MECHANICAL_DESIGN_GEOMETRIC_PRESENTATION_REPRESENTATION('',(#88),#6096);
#66=SHAPE_REPRESENTATION_RELATIONSHIP('SRR','None',#6141,#77);
#77=ADVANCED_BREP_SHAPE_REPRESENTATION('',(#99),#6089);
#88=STYLED_ITEM('',(#6262),#99);
#99=MANIFOLD_SOLID_BREP('Screw',#3597);
#119=FACE_BOUND('',#595,.T.);
#229=PLANE('',#3879);
#230=PLANE('',#3883);
#231=PLANE('',#3884);
#390=FACE_OUTER_BOUND('',#591,.T.);
#391=FACE_OUTER_BOUND('',#592,.T.);
#392=FACE_OUTER_BOUND('',#593,.T.);
#393=FACE_OUTER_BOUND('',#594,.T.);
#394=FACE_OUTER_BOUND('',#596,.T.);
#591=EDGE_LOOP('',(#2900,#2901,#2902,#2903));
#592=EDGE_LOOP('',(#2904));
#593=EDGE_LOOP('',(#2905,#2906,#2907,#2908));
#594=EDGE_LOOP('',(#2909));
#595=EDGE_LOOP('',(#2910));
#596=EDGE_LOOP('',(#2911));
#927=LINE('',#5577,#1306);
#928=LINE('',#5584,#1307);
#1306=VECTOR('',#4548,7.5);
#1307=VECTOR('',#4557,11.);
#1536=CIRCLE('',#3877,7.5);
#1537=CIRCLE('',#3878,7.5);
#1538=CIRCLE('',#3881,10.88225);
#1539=CIRCLE('',#3882,10.88225);
#1756=VERTEX_POINT('',#5574);
#1757=VERTEX_POINT('',#5576);
#1758=VERTEX_POINT('',#5581);
#1759=VERTEX_POINT('',#5583);
#2162=EDGE_CURVE('',#1756,#1756,#1536,.T.);
#2163=EDGE_CURVE('',#1756,#1757,#927,.T.);
#2164=EDGE_CURVE('',#1757,#1757,#1537,.T.);
#2165=EDGE_CURVE('',#1758,#1758,#1538,.T.);
#2166=EDGE_CURVE('',#1758,#1759,#928,.T.);
#2167=EDGE_CURVE('',#1759,#1759,#1539,.F.);
#2900=ORIENTED_EDGE('',*,*,#2162,.F.);
#2901=ORIENTED_EDGE('',*,*,#2163,.T.);
#2902=ORIENTED_EDGE('',*,*,#2164,.F.);
#2903=ORIENTED_EDGE('',*,*,#2163,.F.);
#2904=ORIENTED_EDGE('',*,*,#2162,.T.);
#2905=ORIENTED_EDGE('',*,*,#2165,.F.);
#2906=ORIENTED_EDGE('',*,*,#2166,.T.);
#2907=ORIENTED_EDGE('',*,*,#2167,.F.);
#2908=ORIENTED_EDGE('',*,*,#2166,.F.);
#2909=ORIENTED_EDGE('',*,*,#2167,.T.);
#2910=ORIENTED_EDGE('',*,*,#2164,.T.);
#2911=ORIENTED_EDGE('',*,*,#2165,.T.);
#3383=CYLINDRICAL_SURFACE('',#3876,7.5);
#3384=CYLINDRICAL_SURFACE('',#3880,10.88225);
#3497=ADVANCED_FACE('',(#390),#3383,.T.);
#3498=ADVANCED_FACE('',(#391),#229,.T.);
#3499=ADVANCED_FACE('',(#392),#3384,.T.);
#3500=ADVANCED_FACE('',(#393,#119),#230,.T.);
#3501=ADVANCED_FACE('',(#394),#231,.F.);
#3597=CLOSED_SHELL('',(#3497,#3498,#3499,#3500,#3501));
#3875=AXIS2_PLACEMENT_3D('',#5572,#4542,#4543);
#3876=AXIS2_PLACEMENT_3D('',#5573,#4544,#4545);
#3877=AXIS2_PLACEMENT_3D('',#5575,#4546,#4547);
#3878=AXIS2_PLACEMENT_3D('',#5578,#4549,#4550);
#3879=AXIS2_PLACEMENT_3D('',#5579,#4551,#4552);
#3880=AXIS2_PLACEMENT_3D('',#5580,#4553,#4554);
#3881=AXIS2_PLACEMENT_3D('',#5582,#4555,#4556);
#3882=AXIS2_PLACEMENT_3D('',#5585,#4558,#4559);
#3883=AXIS2_PLACEMENT_3D('',#5586,#4560,#4561);
#3884=AXIS2_PLACEMENT_3D('',#5587,#4562,#4563);
#4542=DIRECTION('axis',(0.,0.,1.));
#4543=DIRECTION('refdir',(1.,0.,0.));
#4544=DIRECTION('center_axis',(0.,1.,0.));
#4545=DIRECTION('ref_axis',(-1.,0.,0.));
#4546=DIRECTION('center_axis',(0.,1.,0.));
#4547=DIRECTION('ref_axis',(-1.,0.,0.));
#4548=DIRECTION('',(0.,-1.,0.));
#4549=DIRECTION('center_axis',(0.,-1.,0.));
#4550=DIRECTION('ref_axis',(-1.,0.,0.));
#4551=DIRECTION('center_axis',(0.,1.,0.));
#4552=DIRECTION('ref_axis',(-1.,0.,0.));
#4553=DIRECTION('center_axis',(0.,-1.,0.));
#4554=DIRECTION('ref_axis',(-1.,0.,0.));
#4555=DIRECTION('center_axis',(0.,-1.,0.));
#4556=DIRECTION('ref_axis',(-1.,0.,0.));
#4557=DIRECTION('',(0.,1.,0.));
#4558=DIRECTION('center_axis',(0.,-1.,0.));
#4559=DIRECTION('ref_axis',(-1.,0.,0.));
#4560=DIRECTION('center_axis',(0.,1.,0.));
#4561=DIRECTION('ref_axis',(-1.,0.,0.));
#4562=DIRECTION('center_axis',(0.,1.,0.));
#4563=DIRECTION('ref_axis',(-1.,0.,0.));
#5572=CARTESIAN_POINT('',(0.,0.,0.));
#5573=CARTESIAN_POINT('Origin',(4.44089209850063E-15,525.425982185852,41.5000000000007));
#5574=CARTESIAN_POINT('',(7.50000000000001,585.425982185852,41.5000000000007));
#5575=CARTESIAN_POINT('Origin',(4.44089209850063E-15,585.425982185852,41.5000000000007));
#5576=CARTESIAN_POINT('',(7.50000000000001,525.425982185852,41.5000000000007));
#5577=CARTESIAN_POINT('',(7.50000000000001,525.425982185852,41.5000000000007));
#5578=CARTESIAN_POINT('Origin',(4.44089209850063E-15,525.425982185852,41.5000000000007));
#5579=CARTESIAN_POINT('Origin',(4.44089209850063E-15,585.425982185852,41.5000000000007));
#5580=CARTESIAN_POINT('Origin',(4.44089209850063E-15,525.425982185852,41.5000000000007));
#5581=CARTESIAN_POINT('',(10.88225,36.9999821858522,41.5000000000007));
#5582=CARTESIAN_POINT('Origin',(4.44089209850063E-15,36.9999821858522,41.5000000000007));
#5583=CARTESIAN_POINT('',(10.88225,525.425982185852,41.5000000000007));
#5584=CARTESIAN_POINT('',(10.88225,525.425982185852,41.5000000000007));
#5585=CARTESIAN_POINT('Origin',(4.44089209850063E-15,525.425982185852,41.5000000000007));
#5586=CARTESIAN_POINT('Origin',(4.44089209850063E-15,525.425982185852,41.5000000000007));
#5587=CARTESIAN_POINT('Origin',(4.44089209850063E-15,36.9999821858522,41.5000000000007));
#6076=UNCERTAINTY_MEASURE_WITH_UNIT(LENGTH_MEASURE(0.01),#6097,
'DISTANCE_ACCURACY_VALUE',
'Maximum model space distance between geometric entities at asserted c
onnectivities');
#6083=UNCERTAINTY_MEASURE_WITH_UNIT(LENGTH_MEASURE(0.01),#6097,
'DISTANCE_ACCURACY_VALUE',
'Maximum model space distance between geometric entities at asserted c
onnectivities');
#6089=(
GEOMETRIC_REPRESENTATION_CONTEXT(3)
GLOBAL_UNCERTAINTY_ASSIGNED_CONTEXT((#6076))
GLOBAL_UNIT_ASSIGNED_CONTEXT((#6097,#6099,#6100))
REPRESENTATION_CONTEXT('','3D')
);
#6096=(
GEOMETRIC_REPRESENTATION_CONTEXT(3)
GLOBAL_UNCERTAINTY_ASSIGNED_CONTEXT((#6083))
GLOBAL_UNIT_ASSIGNED_CONTEXT((#6097,#6099,#6100))
REPRESENTATION_CONTEXT('','3D')
);
#6097=(
LENGTH_UNIT()
NAMED_UNIT(*)
SI_UNIT(.MILLI.,.METRE.)
);
#6099=(
NAMED_UNIT(*)
PLANE_ANGLE_UNIT()
SI_UNIT($,.RADIAN.)
);
#6100=(
NAMED_UNIT(*)
SI_UNIT($,.STERADIAN.)
SOLID_ANGLE_UNIT()
);
#6106=SHAPE_DEFINITION_REPRESENTATION(#6118,#6141);
#6118=PRODUCT_DEFINITION_SHAPE('',$,#6154);
#6141=SHAPE_REPRESENTATION('',(#3875),#6089);
#6148=PRODUCT_DEFINITION_CONTEXT('part definition',#6186,'design');
#6154=PRODUCT_DEFINITION('Screw','Screw',#6166,#6148);
#6166=PRODUCT_DEFINITION_FORMATION('',$,#6193);
#6186=APPLICATION_CONTEXT(
'Core Data for Automotive Mechanical Design Process');
#6187=PRODUCT_CONTEXT('part definition',#6186,'mechanical');
#6193=PRODUCT('Screw','Screw',$,(#6187));
#6256=COLOUR_RGB('Black',0.12,0.14,0.17);
#6257=FILL_AREA_STYLE_COLOUR('',#6256);
#6258=FILL_AREA_STYLE('',(#6257));
#6259=SURFACE_STYLE_FILL_AREA(#6258);
#6260=SURFACE_SIDE_STYLE('',(#6259));
#6261=SURFACE_STYLE_USAGE(.BOTH.,#6260);
#6262=PRESENTATION_STYLE_ASSIGNMENT((#6261));
ENDSEC;
END-ISO-10303-21;
